ISO-10303-21;
HEADER;
/* Generated by software containing ST-Developer
 * from STEP Tools, Inc. (www.steptools.com) 
 */

FILE_DESCRIPTION(
/* description */ ('Five-roller gravity conveyor'),
/* implementation_level */ '2;1');

FILE_NAME(
/* name */ 'Spacer.step',
/* time_stamp */ '2026-10-29T15:36:43-07:00',
/* author */ (''),
/* organization */ (''),
/* preprocessor_version */ 'ST-DEVELOPER v20.2',
/* originating_system */ 'Autodesk Translation Framework v15.17.0.0',
/* authorisation */ '');

FILE_SCHEMA (('AUTOMOTIVE_DESIGN { 1 0 10303 214 3 1 1 }'));
ENDSEC;

DATA;
#10=MECHANICAL_DESIGN_GEOMETRIC_PRESENTATION_REPRESENTATION('',(#332),#7806);
#288=SHAPE_REPRESENTATION_RELATIONSHIP('SRR','None',#7926,#306);
#306=ADVANCED_BREP_SHAPE_REPRESENTATION('',(#357),#7799);
#332=STYLED_ITEM('',(#8084),#357);
#357=MANIFOLD_SOLID_BREP('Body1',#4220);
#393=FACE_BOUND('',#1103,.T.);
#394=FACE_BOUND('',#1105,.T.);
#548=CIRCLE('',#4763,0.505);
#549=CIRCLE('',#4764,0.505);
#550=CIRCLE('',#4766,0.8);
#551=CIRCLE('',#4767,0.8);
#631=CYLINDRICAL_SURFACE('',#4762,0.505);
#632=CYLINDRICAL_SURFACE('',#4765,0.8);
#837=FACE_OUTER_BOUND('',#1100,.T.);
#838=FACE_OUTER_BOUND('',#1101,.T.);
#839=FACE_OUTER_BOUND('',#1102,.T.);
#840=FACE_OUTER_BOUND('',#1104,.T.);
#1100=EDGE_LOOP('',(#3644,#3645,#3646,#3647));
#1101=EDGE_LOOP('',(#3648,#3649,#3650,#3651));
#1102=EDGE_LOOP('',(#3652));
#1103=EDGE_LOOP('',(#3653));
#1104=EDGE_LOOP('',(#3654));
#1105=EDGE_LOOP('',(#3655));
#1473=LINE('',#7515,#1814);
#1474=LINE('',#7521,#1815);
#1814=VECTOR('',#5883,0.505);
#1815=VECTOR('',#5890,0.8);
#2162=VERTEX_POINT('',#7512);
#2163=VERTEX_POINT('',#7514);
#2164=VERTEX_POINT('',#7518);
#2165=VERTEX_POINT('',#7520);
#2665=EDGE_CURVE('',#2162,#2162,#548,.T.);
#2666=EDGE_CURVE('',#2162,#2163,#1473,.T.);
#2667=EDGE_CURVE('',#2163,#2163,#549,.T.);
#2668=EDGE_CURVE('',#2164,#2164,#550,.T.);
#2669=EDGE_CURVE('',#2164,#2165,#1474,.T.);
#2670=EDGE_CURVE('',#2165,#2165,#551,.T.);
#3644=ORIENTED_EDGE('',*,*,#2665,.F.);
#3645=ORIENTED_EDGE('',*,*,#2666,.T.);
#3646=ORIENTED_EDGE('',*,*,#2667,.T.);
#3647=ORIENTED_EDGE('',*,*,#2666,.F.);
#3648=ORIENTED_EDGE('',*,*,#2668,.F.);
#3649=ORIENTED_EDGE('',*,*,#2669,.T.);
#3650=ORIENTED_EDGE('',*,*,#2670,.T.);
#3651=ORIENTED_EDGE('',*,*,#2669,.F.);
#3652=ORIENTED_EDGE('',*,*,#2668,.T.);
#3653=ORIENTED_EDGE('',*,*,#2665,.T.);
#3654=ORIENTED_EDGE('',*,*,#2670,.F.);
#3655=ORIENTED_EDGE('',*,*,#2667,.F.);
#3945=PLANE('',#4768);
#3946=PLANE('',#4769);
#4152=ADVANCED_FACE('',(#837),#631,.F.);
#4153=ADVANCED_FACE('',(#838),#632,.T.);
#4154=ADVANCED_FACE('',(#839,#393),#3945,.T.);
#4155=ADVANCED_FACE('',(#840,#394),#3946,.F.);
#4220=CLOSED_SHELL('',(#4152,#4153,#4154,#4155));
#4761=AXIS2_PLACEMENT_3D('',#7510,#5877,#5878);
#4762=AXIS2_PLACEMENT_3D('',#7511,#5879,#5880);
#4763=AXIS2_PLACEMENT_3D('',#7513,#5881,#5882);
#4764=AXIS2_PLACEMENT_3D('',#7516,#5884,#5885);
#4765=AXIS2_PLACEMENT_3D('',#7517,#5886,#5887);
#4766=AXIS2_PLACEMENT_3D('',#7519,#5888,#5889);
#4767=AXIS2_PLACEMENT_3D('',#7522,#5891,#5892);
#4768=AXIS2_PLACEMENT_3D('',#7523,#5893,#5894);
#4769=AXIS2_PLACEMENT_3D('',#7524,#5895,#5896);
#5877=DIRECTION('axis',(0.,0.,1.));
#5878=DIRECTION('refdir',(1.,0.,0.));
#5879=DIRECTION('center_axis',(0.,1.,0.));
#5880=DIRECTION('ref_axis',(1.,0.,0.));
#5881=DIRECTION('center_axis',(0.,-1.,0.));
#5882=DIRECTION('ref_axis',(1.,0.,0.));
#5883=DIRECTION('',(0.,-1.,0.));
#5884=DIRECTION('center_axis',(0.,-1.,0.));
#5885=DIRECTION('ref_axis',(1.,0.,0.));
#5886=DIRECTION('center_axis',(0.,1.,0.));
#5887=DIRECTION('ref_axis',(1.,0.,0.));
#5888=DIRECTION('center_axis',(0.,1.,0.));
#5889=DIRECTION('ref_axis',(1.,0.,0.));
#5890=DIRECTION('',(0.,-1.,0.));
#5891=DIRECTION('center_axis',(0.,1.,0.));
#5892=DIRECTION('ref_axis',(1.,0.,0.));
#5893=DIRECTION('center_axis',(0.,1.,0.));
#5894=DIRECTION('ref_axis',(1.,0.,0.));
#5895=DIRECTION('center_axis',(0.,1.,0.));
#5896=DIRECTION('ref_axis',(1.,0.,0.));
#7510=CARTESIAN_POINT('',(0.,0.,0.));
#7511=CARTESIAN_POINT('Origin',(0.,-1.6,4.5));
#7512=CARTESIAN_POINT('',(-0.505,0.,4.5));
#7513=CARTESIAN_POINT('Origin',(0.,0.,4.5));
#7514=CARTESIAN_POINT('',(-0.505,-1.6,4.5));
#7515=CARTESIAN_POINT('',(-0.505,-1.6,4.5));
#7516=CARTESIAN_POINT('Origin',(0.,-1.6,4.5));
#7517=CARTESIAN_POINT('Origin',(0.,-1.6,4.5));
#7518=CARTESIAN_POINT('',(-0.8,0.,4.5));
#7519=CARTESIAN_POINT('Origin',(0.,0.,4.5));
#7520=CARTESIAN_POINT('',(-0.8,-1.6,4.5));
#7521=CARTESIAN_POINT('',(-0.8,-1.6,4.5));
#7522=CARTESIAN_POINT('Origin',(0.,-1.6,4.5));
#7523=CARTESIAN_POINT('Origin',(0.,0.,4.5));
#7524=CARTESIAN_POINT('Origin',(0.,-1.6,4.5));
#7775=UNCERTAINTY_MEASURE_WITH_UNIT(LENGTH_MEASURE(0.001),#7807,
'DISTANCE_ACCURACY_VALUE',
'Maximum model space distance between geometric entities at asserted c
onnectivities');
#7782=UNCERTAINTY_MEASURE_WITH_UNIT(LENGTH_MEASURE(0.001),#7807,
'DISTANCE_ACCURACY_VALUE',
'Maximum model space distance between geometric entities at asserted c
onnectivities');
#7799=(
GEOMETRIC_REPRESENTATION_CONTEXT(3)
GLOBAL_UNCERTAINTY_ASSIGNED_CONTEXT((#7775))
GLOBAL_UNIT_ASSIGNED_CONTEXT((#7807,#7809,#7810))
REPRESENTATION_CONTEXT('','3D')
);
#7806=(
GEOMETRIC_REPRESENTATION_CONTEXT(3)
GLOBAL_UNCERTAINTY_ASSIGNED_CONTEXT((#7782))
GLOBAL_UNIT_ASSIGNED_CONTEXT((#7807,#7809,#7810))
REPRESENTATION_CONTEXT('','3D')
);
#7807=(
LENGTH_UNIT()
NAMED_UNIT(*)
SI_UNIT(.CENTI.,.METRE.)
);
#7809=(
NAMED_UNIT(*)
PLANE_ANGLE_UNIT()
SI_UNIT($,.RADIAN.)
);
#7810=(
NAMED_UNIT(*)
SI_UNIT($,.STERADIAN.)
SOLID_ANGLE_UNIT()
);
#7827=SHAPE_DEFINITION_REPRESENTATION(#7855,#7926);
#7855=PRODUCT_DEFINITION_SHAPE('',$,#7950);
#7926=SHAPE_REPRESENTATION('',(#4761),#7799);
#7933=PRODUCT_DEFINITION_CONTEXT('part definition',#8004,'design');
#7950=PRODUCT_DEFINITION('Spacer','Spacer',#7973,#7933);
#7973=PRODUCT_DEFINITION_FORMATION('',$,#8022);
#8004=APPLICATION_CONTEXT(
'Core Data for Automotive Mechanical Design Process');
#8005=PRODUCT_CONTEXT('part definition',#8004,'mechanical');
#8022=PRODUCT('Spacer','Spacer','Spacer',(#8005));
#8078=COLOUR_RGB('Sky Blue',0.24,0.69,0.87);
#8079=FILL_AREA_STYLE_COLOUR('',#8078);
#8080=FILL_AREA_STYLE('',(#8079));
#8081=SURFACE_STYLE_FILL_AREA(#8080);
#8082=SURFACE_SIDE_STYLE('',(#8081));
#8083=SURFACE_STYLE_USAGE(.BOTH.,#8082);
#8084=PRESENTATION_STYLE_ASSIGNMENT((#8083));
ENDSEC;
END-ISO-10303-21;
